ISO-10303-21;
HEADER;
FILE_DESCRIPTION (('STEP AP214'),
    '1' );
FILE_NAME ('output shaft.step',
    '2026-10-08T09:53:37',
    ( '' ),
    ( '' ),
    'SwSTEP 2.0',
    'SolidWorks 2026',
    '' );
FILE_SCHEMA (( 'AUTOMOTIVE_DESIGN' ));
ENDSEC;

DATA;
#35=VECTOR ( 'NONE', #29817, 1000.000000000000000 ) ;
#44=DIRECTION ( 'NONE',  ( 0.000000000000000000, 0.000000000000000000, -1.000000000000000000 ) ) ;
#658=DIRECTION ( 'NONE',  ( 1.000000000000000000, 0.000000000000000000, 0.000000000000000000 ) ) ;
#717=ORIENTED_EDGE ( 'NONE', *, *, #11315, .T. ) ;
#727=ORIENTED_EDGE ( 'NONE', *, *, #31301, .F. ) ;
#916=CARTESIAN_POINT ( 'NONE',  ( 0.000000000000000000, -120.0000000000000000, -40.00000000000000711 ) ) ;
#921=APPLICATION_CONTEXT ( 'automotive_design' ) ;
#1150=ORIENTED_EDGE ( 'NONE', *, *, #57635, .F. ) ;
#1291=VECTOR ( 'NONE', #65356, 1000.000000000000000 ) ;
#1401=EDGE_CURVE ( 'NONE', #32707, #28632, #35106, .T. ) ;
#1659=DIRECTION ( 'NONE',  ( -1.000000000000000000, 0.000000000000000000, 0.000000000000000000 ) ) ;
#1712=ORIENTED_EDGE ( 'NONE', *, *, #1401, .F. ) ;
#1946=DIRECTION ( 'NONE',  ( 1.000000000000000000, 0.000000000000000000, 0.000000000000000000 ) ) ;
#2004=EDGE_CURVE ( 'NONE', #59025, #67396, #36886, .T. ) ;
#2232=ORIENTED_EDGE ( 'NONE', *, *, #11483, .T. ) ;
#2346=ORIENTED_EDGE ( 'NONE', *, *, #61272, .T. ) ;
#2540=EDGE_CURVE ( 'NONE', #32056, #12963, #19470, .T. ) ;
#2596=EDGE_CURVE ( 'NONE', #67396, #13415, #20952, .T. ) ;
#2675=PLANE ( 'NONE',  #31570 ) ;
#3083=ORIENTED_EDGE ( 'NONE', *, *, #51760, .F. ) ;
#3090=ORIENTED_EDGE ( 'NONE', *, *, #57635, .T. ) ;
#3226=DIRECTION ( 'NONE',  ( 0.000000000000000000, 0.000000000000000000, -1.000000000000000000 ) ) ;
#3241=ADVANCED_FACE ( 'NONE', ( #9636 ), #26175, .F. ) ;
#3328=DIRECTION ( 'NONE',  ( -0.000000000000000000, -1.000000000000000000, -0.000000000000000000 ) ) ;
#3568=CARTESIAN_POINT ( 'NONE',  ( 12.50000000000000000, -132.5000000000000000, 40.00000000000000000 ) ) ;
#3786=MECHANICAL_DESIGN_GEOMETRIC_PRESENTATION_REPRESENTATION('',(#37375),#63789);
#3802=ORIENTED_EDGE ( 'NONE', *, *, #30312, .F. ) ;
#3882=DIRECTION ( 'NONE',  ( 0.000000000000000000, 1.000000000000000000, 0.000000000000000000 ) ) ;
#4103=EDGE_CURVE ( 'NONE', #12963, #67396, #69287, .T. ) ;
#4112=ORIENTED_EDGE ( 'NONE', *, *, #22693, .T. ) ;
#4323=LINE ( 'NONE', #37786, #64382 ) ;
#4369=CARTESIAN_POINT ( 'NONE',  ( -12.50000000000000000, -132.5000000000000000, -40.00000000000000000 ) ) ;
#4447=FACE_OUTER_BOUND ( 'NONE', #40989, .T. ) ;
#4598=( GEOMETRIC_REPRESENTATION_CONTEXT ( 3 ) GLOBAL_UNCERTAINTY_ASSIGNED_CONTEXT ( ( #6034 ) ) GLOBAL_UNIT_ASSIGNED_CONTEXT ( ( #60719, #43805, #49782 ) ) REPRESENTATION_CONTEXT ( 'NONE', 'WORKASPACE' ) );
#4743=ORIENTED_EDGE ( 'NONE', *, *, #63274, .T. ) ;
#4769=CIRCLE ( 'NONE', #9571, 12.49999999999999822 ) ;
#5073=( LENGTH_UNIT ( ) NAMED_UNIT ( * ) SI_UNIT ( .MILLI., .METRE. ) );
#5311=EDGE_CURVE ( 'NONE', #28632, #47641, #35501, .T. ) ;
#5610=DIRECTION ( 'NONE',  ( 0.000000000000000000, 0.000000000000000000, 1.000000000000000000 ) ) ;
#5719=ORIENTED_EDGE ( 'NONE', *, *, #72608, .T. ) ;
#5728=EDGE_CURVE ( 'NONE', #13415, #59025, #57195, .T. ) ;
#5819=CARTESIAN_POINT ( 'NONE',  ( -12.50000000000000000, -107.5000000000000000, 40.00000000000000000 ) ) ;
#6022=DIRECTION ( 'NONE',  ( 1.000000000000000000, 0.000000000000000000, 0.000000000000000000 ) ) ;
#6034=UNCERTAINTY_MEASURE_WITH_UNIT (LENGTH_MEASURE( 1.000000000000000082E-05 ), #60719, 'distance_accuracy_value', 'NONE');
#6084=ORIENTED_EDGE ( 'NONE', *, *, #55163, .F. ) ;
#6261=AXIS2_PLACEMENT_3D ( 'NONE', #64685, #14648, #60173 ) ;
#6315=AXIS2_PLACEMENT_3D ( 'NONE', #33790, #5610, #40179 ) ;
#6515=DIRECTION ( 'NONE',  ( 0.000000000000000000, 1.000000000000000000, 0.000000000000000000 ) ) ;
#6797=VECTOR ( 'NONE', #69934, 1000.000000000000000 ) ;
#6921=CARTESIAN_POINT ( 'NONE',  ( -12.50000000000000000, -132.5000000000000000, 40.00000000000000000 ) ) ;
#7268=ORIENTED_EDGE ( 'NONE', *, *, #23172, .T. ) ;
#7323=DIRECTION ( 'NONE',  ( 0.000000000000000000, 1.000000000000000000, 0.000000000000000000 ) ) ;
#7616=PLANE ( 'NONE',  #70312 ) ;
#7651=CIRCLE ( 'NONE', #64071, 12.49999999999999822 ) ;
#7837=EDGE_LOOP ( 'NONE', ( #56875, #59750, #57543, #29754, #19291, #40900 ) ) ;
#8183=CARTESIAN_POINT ( 'NONE',  ( 12.50000000000000000, -107.5000000000000000, -40.00000000000000000 ) ) ;
#8591=ORIENTED_EDGE ( 'NONE', *, *, #21038, .F. ) ;
#8592=CARTESIAN_POINT ( 'NONE',  ( -12.49999999999999822, -120.0000000000000000, 125.0000000000000000 ) ) ;
#8691=DIRECTION ( 'NONE',  ( 0.000000000000000000, 0.000000000000000000, -1.000000000000000000 ) ) ;
#8721=DIRECTION ( 'NONE',  ( 0.000000000000000000, 0.000000000000000000, 1.000000000000000000 ) ) ;
#8840=DIRECTION ( 'NONE',  ( 0.000000000000000000, 0.000000000000000000, -1.000000000000000000 ) ) ;
#9199=SURFACE_STYLE_FILL_AREA ( #44157 ) ;
#9202=PLANE ( 'NONE',  #38241 ) ;
#9254=AXIS2_PLACEMENT_3D ( 'NONE', #29720, #12807, #69952 ) ;
#9293=PRODUCT_DEFINITION_CONTEXT ( 'detailed design', #921, 'design' ) ;
#9492=ADVANCED_FACE ( 'NONE', ( #67085 ), #9202, .T. ) ;
#9500=ADVANCED_FACE ( 'NONE', ( #55063 ), #42680, .T. ) ;
#9516=ORIENTED_EDGE ( 'NONE', *, *, #9683, .T. ) ;
#9571=AXIS2_PLACEMENT_3D ( 'NONE', #16393, #16017, #21657 ) ;
#9636=FACE_OUTER_BOUND ( 'NONE', #20721, .T. ) ;
#9639=VECTOR ( 'NONE', #13985, 1000.000000000000000 ) ;
#9683=EDGE_CURVE ( 'NONE', #27851, #28632, #57471, .T. ) ;
#9798=VECTOR ( 'NONE', #658, 1000.000000000000000 ) ;
#9940=PRESENTATION_STYLE_ASSIGNMENT (( #14840 ) ) ;
#10038=VECTOR ( 'NONE', #45230, 1000.000000000000000 ) ;
#10285=LINE ( 'NONE', #61803, #39466 ) ;
#10317=( NAMED_UNIT ( * ) PLANE_ANGLE_UNIT ( ) SI_UNIT ( $, .RADIAN. ) );
#10673=CARTESIAN_POINT ( 'NONE',  ( -12.50000000000000000, -107.5000000000000000, -40.00000000000000000 ) ) ;
#10698=DIRECTION ( 'NONE',  ( 0.000000000000000000, 0.000000000000000000, -1.000000000000000000 ) ) ;
#10812=CYLINDRICAL_SURFACE ( 'NONE', #56071, 12.49999999999999822 ) ;
#10903=CARTESIAN_POINT ( 'NONE',  ( -12.50000000000000000, -132.5000000000000000, 40.00000000000000000 ) ) ;
#10986=DIRECTION ( 'NONE',  ( -1.000000000000000000, 0.000000000000000000, 0.000000000000000000 ) ) ;
#11067=( NAMED_UNIT ( * ) SI_UNIT ( $, .STERADIAN. ) SOLID_ANGLE_UNIT ( ) );
#11214=PLANE ( 'NONE',  #21911 ) ;
#11315=EDGE_CURVE ( 'NONE', #13415, #21312, #40827, .T. ) ;
#11483=EDGE_CURVE ( 'NONE', #53012, #32056, #61719, .T. ) ;
#11518=LINE ( 'NONE', #62303, #9798 ) ;
#11699=AXIS2_PLACEMENT_3D ( 'NONE', #20577, #43530, #27305 ) ;
#11981=CARTESIAN_POINT ( 'NONE',  ( 0.000000000000000000, -120.0000000000000000, 125.0000000000000000 ) ) ;
#12132=DIRECTION ( 'NONE',  ( -0.000000000000000000, -1.000000000000000000, -0.000000000000000000 ) ) ;
#12198=ADVANCED_FACE ( 'NONE', ( #72066 ), #49509, .T. ) ;
#12313=CARTESIAN_POINT ( 'NONE',  ( 12.49999999999999822, -120.0000000000000000, -125.0000000000000000 ) ) ;
#12651=MANIFOLD_SOLID_BREP ( 'Boss-Extrude2', #46426 ) ;
#12718=ORIENTED_EDGE ( 'NONE', *, *, #35580, .F. ) ;
#12807=DIRECTION ( 'NONE',  ( 0.000000000000000000, 0.000000000000000000, -1.000000000000000000 ) ) ;
#12963=VERTEX_POINT ( 'NONE', #18176 ) ;
#13370=LINE ( 'NONE', #30652, #60461 ) ;
#13415=VERTEX_POINT ( 'NONE', #6921 ) ;
#13748=VECTOR ( 'NONE', #45302, 1000.000000000000000 ) ;
#13822=VECTOR ( 'NONE', #3328, 1000.000000000000000 ) ;
#13985=DIRECTION ( 'NONE',  ( -0.000000000000000000, -0.000000000000000000, -1.000000000000000000 ) ) ;
#13988=DIRECTION ( 'NONE',  ( 0.000000000000000000, 0.000000000000000000, -1.000000000000000000 ) ) ;
#14215=LINE ( 'NONE', #8592, #48916 ) ;
#14473=CARTESIAN_POINT ( 'NONE',  ( 0.000000000000000000, 0.000000000000000000, -40.00000000000000000 ) ) ;
#14638=DIRECTION ( 'NONE',  ( 1.000000000000000000, 0.000000000000000000, 0.000000000000000000 ) ) ;
#14648=DIRECTION ( 'NONE',  ( 0.000000000000000000, 0.000000000000000000, -1.000000000000000000 ) ) ;
#14833=ADVANCED_FACE ( 'NONE', ( #68372 ), #11214, .F. ) ;
#14840=SURFACE_STYLE_USAGE ( .BOTH. , #71974 ) ;
#15081=EDGE_LOOP ( 'NONE', ( #20545, #1712, #22785 ) ) ;
#15176=UNCERTAINTY_MEASURE_WITH_UNIT (LENGTH_MEASURE( 1.000000000000000082E-05 ), #38524, 'distance_accuracy_value', 'NONE');
#15180=DIRECTION ( 'NONE',  ( 0.000000000000000000, 1.000000000000000000, 0.000000000000000000 ) ) ;
#15675=CARTESIAN_POINT ( 'NONE',  ( -12.50000000000000000, -120.0000000000000000, 40.00000000000000711 ) ) ;
#15796=PLANE ( 'NONE',  #53547 ) ;
#15858=CARTESIAN_POINT ( 'NONE',  ( -12.50000000000000000, -120.0000000000000000, -40.00000000000000711 ) ) ;
#16017=DIRECTION ( 'NONE',  ( 0.000000000000000000, 0.000000000000000000, 1.000000000000000000 ) ) ;
#16238=APPLICATION_CONTEXT ( 'automotive_design' ) ;
#16274=EDGE_CURVE ( 'NONE', #67396, #32056, #38882, .T. ) ;
#16393=CARTESIAN_POINT ( 'NONE',  ( 0.000000000000000000, -120.0000000000000000, 125.0000000000000000 ) ) ;
#16531=FACE_OUTER_BOUND ( 'NONE', #25165, .T. ) ;
#16705=SURFACE_STYLE_FILL_AREA ( #27972 ) ;
#16826=FACE_OUTER_BOUND ( 'NONE', #45131, .T. ) ;
#16865=CARTESIAN_POINT ( 'NONE',  ( 0.000000000000000000, 0.000000000000000000, 40.00000000000000000 ) ) ;
#16911=CARTESIAN_POINT ( 'NONE',  ( 12.50000000000000000, -107.5000000000000000, 40.00000000000000000 ) ) ;
#17118=LINE ( 'NONE', #64465, #50663 ) ;
#17334=EDGE_CURVE ( 'NONE', #21312, #27851, #22387, .T. ) ;
#18176=CARTESIAN_POINT ( 'NONE',  ( -12.50000000000000000, -107.5000000000000000, 40.00000000000000000 ) ) ;
#18300=VERTEX_POINT ( 'NONE', #12313 ) ;
#18333=FACE_OUTER_BOUND ( 'NONE', #7837, .T. ) ;
#18500=FACE_OUTER_BOUND ( 'NONE', #31880, .T. ) ;
#18833=AXIS2_PLACEMENT_3D ( 'NONE', #21762, #62001, #67261 ) ;
#18959=LINE ( 'NONE', #41907, #21871 ) ;
#19166=DIRECTION ( 'NONE',  ( 0.000000000000000000, 0.000000000000000000, 1.000000000000000000 ) ) ;
#19291=ORIENTED_EDGE ( 'NONE', *, *, #49289, .T. ) ;
#19470=LINE ( 'NONE', #42414, #1291 ) ;
#19692=CARTESIAN_POINT ( 'NONE',  ( 0.000000000000000000, -132.5000000000000000, 40.00000000000000711 ) ) ;
#19735=DIRECTION ( 'NONE',  ( 1.000000000000000000, 0.000000000000000000, 0.000000000000000000 ) ) ;
#20164=DIRECTION ( 'NONE',  ( 0.000000000000000000, 0.000000000000000000, 1.000000000000000000 ) ) ;
#20316=ORIENTED_EDGE ( 'NONE', *, *, #66871, .T. ) ;
#20545=ORIENTED_EDGE ( 'NONE', *, *, #5311, .F. ) ;
#20577=CARTESIAN_POINT ( 'NONE',  ( 0.000000000000000000, 0.000000000000000000, -40.00000000000000000 ) ) ;
#20721=EDGE_LOOP ( 'NONE', ( #61146, #57412 ) ) ;
#20952=LINE ( 'NONE', #38248, #13822 ) ;
#21038=EDGE_CURVE ( 'NONE', #73511, #39300, #55039, .T. ) ;
#21134=CARTESIAN_POINT ( 'NONE',  ( 0.000000000000000000, -120.0000000000000000, 40.00000000000000711 ) ) ;
#21312=VERTEX_POINT ( 'NONE', #37949 ) ;
#21426=DIRECTION ( 'NONE',  ( -1.000000000000000000, 0.000000000000000000, 0.000000000000000000 ) ) ;
#21475=EDGE_CURVE ( 'NONE', #22889, #58924, #67535, .T. ) ;
#21590=PRESENTATION_STYLE_ASSIGNMENT (( #45667 ) ) ;
#21657=DIRECTION ( 'NONE',  ( 1.000000000000000000, 0.000000000000000000, 0.000000000000000000 ) ) ;
#21762=CARTESIAN_POINT ( 'NONE',  ( 0.000000000000000000, 0.000000000000000000, -40.00000000000000000 ) ) ;
#21871=VECTOR ( 'NONE', #58447, 1000.000000000000000 ) ;
#21911=AXIS2_PLACEMENT_3D ( 'NONE', #16865, #46173, #39795 ) ;
#21978=DIRECTION ( 'NONE',  ( -0.000000000000000000, -0.000000000000000000, -1.000000000000000000 ) ) ;
#22067=ADVANCED_FACE ( 'NONE', ( #71873 ), #48223, .T. ) ;
#22183=VECTOR ( 'NONE', #45864, 1000.000000000000000 ) ;
#22288=CARTESIAN_POINT ( 'NONE',  ( 12.50000000000000000, -107.5000000000000000, 40.00000000000000000 ) ) ;
#22387=LINE ( 'NONE', #4369, #29054 ) ;
#22450=ORIENTED_EDGE ( 'NONE', *, *, #52910, .F. ) ;
#22532=CARTESIAN_POINT ( 'NONE',  ( -12.49999999999999822, -120.0000000000000000, 125.0000000000000000 ) ) ;
#22663=LINE ( 'NONE', #22288, #10038 ) ;
#22693=EDGE_CURVE ( 'NONE', #32056, #39300, #45869, .T. ) ;
#22785=ORIENTED_EDGE ( 'NONE', *, *, #49289, .F. ) ;
#22889=VERTEX_POINT ( 'NONE', #22532 ) ;
#23065=EDGE_LOOP ( 'NONE', ( #60860, #3083, #24859 ) ) ;
#23172=EDGE_CURVE ( 'NONE', #65045, #35341, #17118, .T. ) ;
#23745=PRODUCT_DEFINITION ( 'UNKNOWN', '', #36436, #9293 ) ;
#23799=ORIENTED_EDGE ( 'NONE', *, *, #21475, .T. ) ;
#23988=CARTESIAN_POINT ( 'NONE',  ( -12.50000000000000000, -107.5000000000000000, 40.00000000000000000 ) ) ;
#24185=DIRECTION ( 'NONE',  ( 0.000000000000000000, 0.000000000000000000, -1.000000000000000000 ) ) ;
#24595=ORIENTED_EDGE ( 'NONE', *, *, #16274, .F. ) ;
#24859=ORIENTED_EDGE ( 'NONE', *, *, #23172, .F. ) ;
#24908=DIRECTION ( 'NONE',  ( -1.000000000000000000, 0.000000000000000000, 0.000000000000000000 ) ) ;
#24991=CARTESIAN_POINT ( 'NONE',  ( 0.000000000000000000, -107.5000000000000000, -40.00000000000000711 ) ) ;
#25035=AXIS2_PLACEMENT_3D ( 'NONE', #62975, #10698, #51285 ) ;
#25165=EDGE_LOOP ( 'NONE', ( #42822, #44489, #48945, #37122, #37127, #56330 ) ) ;
#25394=DIRECTION ( 'NONE',  ( -1.000000000000000000, 0.000000000000000000, -0.000000000000000000 ) ) ;
#26076=CARTESIAN_POINT ( 'NONE',  ( 12.49999999999999822, -120.0000000000000000, 125.0000000000000000 ) ) ;
#26113=FILL_AREA_STYLE_COLOUR ( '', #47830 ) ;
#26175=PLANE ( 'NONE',  #63431 ) ;
#26200=CIRCLE ( 'NONE', #35808, 12.49999999999999822 ) ;
#26466=DIRECTION ( 'NONE',  ( 0.000000000000000000, 1.000000000000000000, 0.000000000000000000 ) ) ;
#26482=DIRECTION ( 'NONE',  ( -1.000000000000000000, -0.000000000000000000, -0.000000000000000000 ) ) ;
#27305=DIRECTION ( 'NONE',  ( -1.000000000000000000, 0.000000000000000000, -0.000000000000000000 ) ) ;
#27729=DIRECTION ( 'NONE',  ( -1.000000000000000000, 0.000000000000000000, 0.000000000000000000 ) ) ;
#27851=VERTEX_POINT ( 'NONE', #62002 ) ;
#27965=DIRECTION ( 'NONE',  ( -0.000000000000000000, -0.000000000000000000, -1.000000000000000000 ) ) ;
#27972=FILL_AREA_STYLE ('',( #44917 ) ) ;
#28094=DIRECTION ( 'NONE',  ( -0.000000000000000000, -0.000000000000000000, -1.000000000000000000 ) ) ;
#28340=SHAPE_REPRESENTATION_RELATIONSHIP ( 'NONE' , 'NONE' ,  #66992, #68699 ) ;
#28525=DIRECTION ( 'NONE',  ( -1.000000000000000000, 0.000000000000000000, 0.000000000000000000 ) ) ;
#28632=VERTEX_POINT ( 'NONE', #15858 ) ;
#29054=VECTOR ( 'NONE', #33661, 1000.000000000000000 ) ;
#29720=CARTESIAN_POINT ( 'NONE',  ( 0.000000000000000000, -120.0000000000000000, 40.00000000000000711 ) ) ;
#29754=ORIENTED_EDGE ( 'NONE', *, *, #51760, .T. ) ;
#29817=DIRECTION ( 'NONE',  ( -0.000000000000000000, -1.000000000000000000, -0.000000000000000000 ) ) ;
#30169=CARTESIAN_POINT ( 'NONE',  ( -12.50000000000000000, -132.5000000000000000, 40.00000000000000000 ) ) ;
#30312=EDGE_CURVE ( 'NONE', #59025, #73511, #48141, .T. ) ;
#30515=DIRECTION ( 'NONE',  ( 0.000000000000000000, 0.000000000000000000, -1.000000000000000000 ) ) ;
#30523=CARTESIAN_POINT ( 'NONE',  ( 12.50000000000000000, -132.5000000000000000, 40.00000000000000000 ) ) ;
#30652=CARTESIAN_POINT ( 'NONE',  ( -12.50000000000000000, -107.5000000000000000, -40.00000000000000000 ) ) ;
#30846=AXIS2_PLACEMENT_3D ( 'NONE', #60157, #19166, #14638 ) ;
#30911=DIRECTION ( 'NONE',  ( -0.000000000000000000, -0.000000000000000000, -1.000000000000000000 ) ) ;
#31288=DIRECTION ( 'NONE',  ( -1.000000000000000000, 0.000000000000000000, 0.000000000000000000 ) ) ;
#31301=EDGE_CURVE ( 'NONE', #39300, #59025, #37220, .T. ) ;
#31570=AXIS2_PLACEMENT_3D ( 'NONE', #71406, #43971, #54504 ) ;
#31692=ORIENTED_EDGE ( 'NONE', *, *, #72608, .F. ) ;
#31880=EDGE_LOOP ( 'NONE', ( #47272, #68982, #33931 ) ) ;
#32056=VERTEX_POINT ( 'NONE', #43469 ) ;
#32075=ORIENTED_EDGE ( 'NONE', *, *, #17334, .T. ) ;
#32577=VECTOR ( 'NONE', #12132, 1000.000000000000000 ) ;
#32707=VERTEX_POINT ( 'NONE', #38456 ) ;
#33125=ORIENTED_EDGE ( 'NONE', *, *, #31301, .T. ) ;
#33661=DIRECTION ( 'NONE',  ( 1.000000000000000000, 0.000000000000000000, 0.000000000000000000 ) ) ;
#33678=VECTOR ( 'NONE', #72969, 1000.000000000000000 ) ;
#33790=CARTESIAN_POINT ( 'NONE',  ( 0.000000000000000000, -120.0000000000000000, 125.0000000000000000 ) ) ;
#33931=ORIENTED_EDGE ( 'NONE', *, *, #2596, .T. ) ;
#33997=CARTESIAN_POINT ( 'NONE',  ( -12.49999999999999822, -120.0000000000000000, -125.0000000000000000 ) ) ;
#33999=CARTESIAN_POINT ( 'NONE',  ( -12.49999999999999822, -120.0000000000000000, 125.0000000000000000 ) ) ;
#34011=EDGE_CURVE ( 'NONE', #53012, #35341, #22663, .T. ) ;
#34043=AXIS2_PLACEMENT_3D ( 'NONE', #73305, #8691, #21426 ) ;
#34259=FACE_OUTER_BOUND ( 'NONE', #41497, .T. ) ;
#34421=EDGE_LOOP ( 'NONE', ( #55671, #56869, #42653 ) ) ;
#34925=FACE_OUTER_BOUND ( 'NONE', #57913, .T. ) ;
#35058=PRODUCT_CONTEXT ( 'NONE', #16238, 'mechanical' ) ;
#35083=ADVANCED_FACE ( 'NONE', ( #34925 ), #63144, .T. ) ;
#35087=AXIS2_PLACEMENT_3D ( 'NONE', #54237, #13988, #24908 ) ;
#35106=LINE ( 'NONE', #58400, #35 ) ;
#35270=ORIENTED_EDGE ( 'NONE', *, *, #63274, .F. ) ;
#35341=VERTEX_POINT ( 'NONE', #8183 ) ;
#35501=CIRCLE ( 'NONE', #36735, 12.49999999999999822 ) ;
#35511=ORIENTED_EDGE ( 'NONE', *, *, #34011, .F. ) ;
#35580=EDGE_CURVE ( 'NONE', #27851, #62613, #11518, .T. ) ;
#35795=CARTESIAN_POINT ( 'NONE',  ( -12.50000000000000000, -132.5000000000000000, 40.00000000000000000 ) ) ;
#35808=AXIS2_PLACEMENT_3D ( 'NONE', #46115, #57392, #57766 ) ;
#35845=EDGE_LOOP ( 'NONE', ( #23799, #5719 ) ) ;
#35954=CARTESIAN_POINT ( 'NONE',  ( 12.50000000000000000, -120.0000000000000000, 40.00000000000000711 ) ) ;
#36249=CIRCLE ( 'NONE', #35087, 12.49999999999999822 ) ;
#36436=PRODUCT_DEFINITION_FORMATION_WITH_SPECIFIED_SOURCE ( 'ANY', '', #66792, .NOT_KNOWN. ) ;
#36735=AXIS2_PLACEMENT_3D ( 'NONE', #916, #24185, #1659 ) ;
#36865=ORIENTED_EDGE ( 'NONE', *, *, #67848, .T. ) ;
#36886=CIRCLE ( 'NONE', #9254, 12.49999999999999822 ) ;
#37040=CARTESIAN_POINT ( 'NONE',  ( 0.000000000000000000, 0.000000000000000000, -40.00000000000000000 ) ) ;
#37103=CARTESIAN_POINT ( 'NONE',  ( 0.000000000000000000, -120.0000000000000000, -125.0000000000000000 ) ) ;
#37122=ORIENTED_EDGE ( 'NONE', *, *, #1401, .T. ) ;
#37127=ORIENTED_EDGE ( 'NONE', *, *, #52910, .T. ) ;
#37220=CIRCLE ( 'NONE', #46827, 12.49999999999999822 ) ;
#37375=STYLED_ITEM ( 'NONE', ( #21590 ), #68699 ) ;
#37448=AXIS2_PLACEMENT_3D ( 'NONE', #62714, #28094, #27729 ) ;
#37786=CARTESIAN_POINT ( 'NONE',  ( 12.49999999999999822, -120.0000000000000000, 125.0000000000000000 ) ) ;
#37949=CARTESIAN_POINT ( 'NONE',  ( -12.50000000000000000, -132.5000000000000000, -40.00000000000000000 ) ) ;
#38015=ADVANCED_FACE ( 'NONE', ( #16531 ), #15796, .F. ) ;
#38241=AXIS2_PLACEMENT_3D ( 'NONE', #37040, #8840, #43446 ) ;
#38248=CARTESIAN_POINT ( 'NONE',  ( -12.50000000000000000, -132.5000000000000000, 40.00000000000000000 ) ) ;
#38456=CARTESIAN_POINT ( 'NONE',  ( -12.50000000000000000, -107.5000000000000000, -40.00000000000000000 ) ) ;
#38524=( LENGTH_UNIT ( ) NAMED_UNIT ( * ) SI_UNIT ( .MILLI., .METRE. ) );
#38537=ADVANCED_FACE ( 'NONE', ( #16826 ), #10812, .T. ) ;
#38815=CARTESIAN_POINT ( 'NONE',  ( 12.50000000000000000, -132.5000000000000000, -40.00000000000000000 ) ) ;
#38882=CIRCLE ( 'NONE', #34043, 12.49999999999999822 ) ;
#39063=EDGE_CURVE ( 'NONE', #22889, #67396, #14215, .T. ) ;
#39300=VERTEX_POINT ( 'NONE', #35954 ) ;
#39466=VECTOR ( 'NONE', #15180, 1000.000000000000000 ) ;
#39542=DIRECTION ( 'NONE',  ( 0.000000000000000000, 0.000000000000000000, -1.000000000000000000 ) ) ;
#39664=EDGE_LOOP ( 'NONE', ( #2232, #4112, #4743 ) ) ;
#39729=CARTESIAN_POINT ( 'NONE',  ( 0.000000000000000000, 0.000000000000000000, 40.00000000000000000 ) ) ;
#39764=CARTESIAN_POINT ( 'NONE',  ( 0.000000000000000000, -120.0000000000000000, 125.0000000000000000 ) ) ;
#39795=DIRECTION ( 'NONE',  ( -1.000000000000000000, 0.000000000000000000, -0.000000000000000000 ) ) ;
#40179=DIRECTION ( 'NONE',  ( 1.000000000000000000, 0.000000000000000000, 0.000000000000000000 ) ) ;
#40616=ORIENTED_EDGE ( 'NONE', *, *, #56784, .F. ) ;
#40827=LINE ( 'NONE', #65152, #9639 ) ;
#40900=ORIENTED_EDGE ( 'NONE', *, *, #57563, .F. ) ;
#40911=DIRECTION ( 'NONE',  ( 0.000000000000000000, -0.000000000000000000, -1.000000000000000000 ) ) ;
#40989=EDGE_LOOP ( 'NONE', ( #43106, #60075, #2346, #1150, #59349 ) ) ;
#41245=CARTESIAN_POINT ( 'NONE',  ( 12.50000000000000000, -132.5000000000000000, -40.00000000000000000 ) ) ;
#41497=EDGE_LOOP ( 'NONE', ( #69838, #33125, #43025 ) ) ;
#41584=EDGE_LOOP ( 'NONE', ( #31692, #36865, #42301, #24595, #45608 ) ) ;
#41891=ORIENTED_EDGE ( 'NONE', *, *, #9683, .F. ) ;
#41907=CARTESIAN_POINT ( 'NONE',  ( 12.49999999999999822, -120.0000000000000000, 125.0000000000000000 ) ) ;
#42211=FACE_OUTER_BOUND ( 'NONE', #63905, .T. ) ;
#42265=ADVANCED_FACE ( 'NONE', ( #45750 ), #63398, .F. ) ;
#42301=ORIENTED_EDGE ( 'NONE', *, *, #22693, .F. ) ;
#42414=CARTESIAN_POINT ( 'NONE',  ( -12.50000000000000000, -107.5000000000000000, 40.00000000000000000 ) ) ;
#42653=ORIENTED_EDGE ( 'NONE', *, *, #2540, .T. ) ;
#42680=PLANE ( 'NONE',  #53861 ) ;
#42822=ORIENTED_EDGE ( 'NONE', *, *, #2596, .F. ) ;
#43025=ORIENTED_EDGE ( 'NONE', *, *, #30312, .T. ) ;
#43106=ORIENTED_EDGE ( 'NONE', *, *, #55346, .T. ) ;
#43147=AXIS2_PLACEMENT_3D ( 'NONE', #39729, #52463, #74297 ) ;
#43289=ADVANCED_FACE ( 'NONE', ( #34259 ), #50439, .F. ) ;
#43395=AXIS2_PLACEMENT_3D ( 'NONE', #48320, #71232, #19735 ) ;
#43446=DIRECTION ( 'NONE',  ( -1.000000000000000000, 0.000000000000000000, -0.000000000000000000 ) ) ;
#43469=CARTESIAN_POINT ( 'NONE',  ( 0.000000000000000000, -107.5000000000000000, 40.00000000000000711 ) ) ;
#43530=DIRECTION ( 'NONE',  ( 0.000000000000000000, 0.000000000000000000, -1.000000000000000000 ) ) ;
#43707=CARTESIAN_POINT ( 'NONE',  ( 0.000000000000000000, -120.0000000000000000, -40.00000000000000711 ) ) ;
#43805=( NAMED_UNIT ( * ) PLANE_ANGLE_UNIT ( ) SI_UNIT ( $, .RADIAN. ) );
#43963=PLANE ( 'NONE',  #18833 ) ;
#43971=DIRECTION ( 'NONE',  ( 0.000000000000000000, 0.000000000000000000, 1.000000000000000000 ) ) ;
#44157=FILL_AREA_STYLE ('',( #26113 ) ) ;
#44489=ORIENTED_EDGE ( 'NONE', *, *, #4103, .F. ) ;
#44813=CARTESIAN_POINT ( 'NONE',  ( 0.000000000000000000, 0.000000000000000000, 40.00000000000000000 ) ) ;
#44901=LINE ( 'NONE', #10673, #56768 ) ;
#44917=FILL_AREA_STYLE_COLOUR ( '', #62607 ) ;
#45052=ORIENTED_EDGE ( 'NONE', *, *, #45154, .F. ) ;
#45082=FACE_OUTER_BOUND ( 'NONE', #53655, .T. ) ;
#45131=EDGE_LOOP ( 'NONE', ( #6084, #51602, #9516, #3090, #68812 ) ) ;
#45154=EDGE_CURVE ( 'NONE', #62613, #65045, #61003, .T. ) ;
#45226=PRODUCT_DEFINITION_SHAPE ( 'NONE', 'NONE',  #23745 ) ;
#45230=DIRECTION ( 'NONE',  ( -0.000000000000000000, -0.000000000000000000, -1.000000000000000000 ) ) ;
#45292=( NAMED_UNIT ( * ) PLANE_ANGLE_UNIT ( ) SI_UNIT ( $, .RADIAN. ) );
#45302=DIRECTION ( 'NONE',  ( -0.000000000000000000, -0.000000000000000000, -1.000000000000000000 ) ) ;
#45463=CARTESIAN_POINT ( 'NONE',  ( 12.50000000000000000, -132.5000000000000000, 40.00000000000000000 ) ) ;
#45608=ORIENTED_EDGE ( 'NONE', *, *, #39063, .F. ) ;
#45667=SURFACE_STYLE_USAGE ( .BOTH. , #61835 ) ;
#45750=FACE_OUTER_BOUND ( 'NONE', #34421, .T. ) ;
#45864=DIRECTION ( 'NONE',  ( -0.000000000000000000, -1.000000000000000000, -0.000000000000000000 ) ) ;
#45869=CIRCLE ( 'NONE', #6261, 12.49999999999999822 ) ;
#46115=CARTESIAN_POINT ( 'NONE',  ( 0.000000000000000000, -120.0000000000000000, -125.0000000000000000 ) ) ;
#46173=DIRECTION ( 'NONE',  ( 0.000000000000000000, 0.000000000000000000, -1.000000000000000000 ) ) ;
#46425=ORIENTED_EDGE ( 'NONE', *, *, #67848, .F. ) ;
#46426=CLOSED_SHELL ( 'NONE', ( #48528, #22067, #35083, #49507, #63502, #65636, #38015, #66137, #42265, #14833, #43289, #9500, #12198, #61464, #46768, #9492, #3241, #38537 ) ) ;
#46768=ADVANCED_FACE ( 'NONE', ( #18500 ), #64383, .F. ) ;
#46827=AXIS2_PLACEMENT_3D ( 'NONE', #21134, #56105, #10986 ) ;
#47242=DIRECTION ( 'NONE',  ( -1.000000000000000000, 0.000000000000000000, 0.000000000000000000 ) ) ;
#47272=ORIENTED_EDGE ( 'NONE', *, *, #5728, .T. ) ;
#47336=ORIENTED_EDGE ( 'NONE', *, *, #39063, .T. ) ;
#47641=VERTEX_POINT ( 'NONE', #24991 ) ;
#47830=COLOUR_RGB ( '', 0.72549020, 0.75294118, 0.79215686) ;
#48141=LINE ( 'NONE', #53409, #57501 ) ;
#48223=CYLINDRICAL_SURFACE ( 'NONE', #58999, 12.49999999999999822 ) ;
#48320=CARTESIAN_POINT ( 'NONE',  ( 0.000000000000000000, 0.000000000000000000, 0.000000000000000000 ) ) ;
#48528=ADVANCED_FACE ( 'NONE', ( #4447 ), #72466, .T. ) ;
#48561=CARTESIAN_POINT ( 'NONE',  ( 0.000000000000000000, 0.000000000000000000, 40.00000000000000000 ) ) ;
#48916=VECTOR ( 'NONE', #60114, 1000.000000000000000 ) ;
#48942=CARTESIAN_POINT ( 'NONE',  ( 0.000000000000000000, -120.0000000000000000, 125.0000000000000000 ) ) ;
#48945=ORIENTED_EDGE ( 'NONE', *, *, #57563, .T. ) ;
#49014=UNCERTAINTY_MEASURE_WITH_UNIT (LENGTH_MEASURE( 1.000000000000000082E-05 ), #5073, 'distance_accuracy_value', 'NONE');
#49289=EDGE_CURVE ( 'NONE', #47641, #32707, #44901, .T. ) ;
#49326=DIRECTION ( 'NONE',  ( 0.000000000000000000, 0.000000000000000000, -1.000000000000000000 ) ) ;
#49507=ADVANCED_FACE ( 'NONE', ( #61264 ), #2675, .T. ) ;
#49509=PLANE ( 'NONE',  #11699 ) ;
#49782=( NAMED_UNIT ( * ) SI_UNIT ( $, .STERADIAN. ) SOLID_ANGLE_UNIT ( ) );
#49954=DIRECTION ( 'NONE',  ( -0.000000000000000000, -0.000000000000000000, -1.000000000000000000 ) ) ;
#50041=CARTESIAN_POINT ( 'NONE',  ( -12.50000000000000000, -107.5000000000000000, 40.00000000000000000 ) ) ;
#50428=VECTOR ( 'NONE', #3882, 1000.000000000000000 ) ;
#50439=PLANE ( 'NONE',  #52633 ) ;
#50663=VECTOR ( 'NONE', #7323, 1000.000000000000000 ) ;
#50762=ORIENTED_EDGE ( 'NONE', *, *, #17334, .F. ) ;
#50801=DIRECTION ( 'NONE',  ( -1.000000000000000000, 0.000000000000000000, 0.000000000000000000 ) ) ;
#50898=ORIENTED_EDGE ( 'NONE', *, *, #5728, .F. ) ;
#50953=VECTOR ( 'NONE', #21978, 1000.000000000000000 ) ;
#51146=CARTESIAN_POINT ( 'NONE',  ( 12.50000000000000000, -120.0000000000000000, -40.00000000000000711 ) ) ;
#51285=DIRECTION ( 'NONE',  ( -1.000000000000000000, 0.000000000000000000, 0.000000000000000000 ) ) ;
#51602=ORIENTED_EDGE ( 'NONE', *, *, #56784, .T. ) ;
#51760=EDGE_CURVE ( 'NONE', #35341, #47641, #13370, .T. ) ;
#51981=VERTEX_POINT ( 'NONE', #33997 ) ;
#52172=ORIENTED_EDGE ( 'NONE', *, *, #21475, .F. ) ;
#52463=DIRECTION ( 'NONE',  ( 0.000000000000000000, 0.000000000000000000, -1.000000000000000000 ) ) ;
#52593=MECHANICAL_DESIGN_GEOMETRIC_PRESENTATION_REPRESENTATION('',(#61027),#4598);
#52633=AXIS2_PLACEMENT_3D ( 'NONE', #44813, #39542, #67740 ) ;
#52910=EDGE_CURVE ( 'NONE', #28632, #21312, #57868, .T. ) ;
#53010=AXIS2_PLACEMENT_3D ( 'NONE', #23988, #69114, #40911 ) ;
#53012=VERTEX_POINT ( 'NONE', #16911 ) ;
#53049=VECTOR ( 'NONE', #26466, 1000.000000000000000 ) ;
#53409=CARTESIAN_POINT ( 'NONE',  ( -12.50000000000000000, -132.5000000000000000, 40.00000000000000000 ) ) ;
#53422=VECTOR ( 'NONE', #49954, 1000.000000000000000 ) ;
#53547=AXIS2_PLACEMENT_3D ( 'NONE', #10903, #6022, #44 ) ;
#53655=EDGE_LOOP ( 'NONE', ( #40616, #45052, #12718 ) ) ;
#53827=DIRECTION ( 'NONE',  ( -1.000000000000000000, 0.000000000000000000, -0.000000000000000000 ) ) ;
#53861=AXIS2_PLACEMENT_3D ( 'NONE', #14473, #3226, #25394 ) ;
#54237=CARTESIAN_POINT ( 'NONE',  ( 0.000000000000000000, -120.0000000000000000, -40.00000000000000711 ) ) ;
#54504=DIRECTION ( 'NONE',  ( 1.000000000000000000, 0.000000000000000000, -0.000000000000000000 ) ) ;
#54934=ORIENTED_EDGE ( 'NONE', *, *, #2004, .F. ) ;
#55039=LINE ( 'NONE', #3568, #53049 ) ;
#55063=FACE_OUTER_BOUND ( 'NONE', #15081, .T. ) ;
#55163=EDGE_CURVE ( 'NONE', #65045, #18300, #18959, .T. ) ;
#55346=EDGE_CURVE ( 'NONE', #47641, #65045, #36249, .T. ) ;
#55671=ORIENTED_EDGE ( 'NONE', *, *, #4103, .T. ) ;
#55978=LINE ( 'NONE', #45463, #53422 ) ;
#56071=AXIS2_PLACEMENT_3D ( 'NONE', #39764, #68707, #47242 ) ;
#56105=DIRECTION ( 'NONE',  ( 0.000000000000000000, 0.000000000000000000, -1.000000000000000000 ) ) ;
#56330=ORIENTED_EDGE ( 'NONE', *, *, #11315, .F. ) ;
#56768=VECTOR ( 'NONE', #26482, 1000.000000000000000 ) ;
#56784=EDGE_CURVE ( 'NONE', #65045, #27851, #7651, .T. ) ;
#56869=ORIENTED_EDGE ( 'NONE', *, *, #16274, .T. ) ;
#56875=ORIENTED_EDGE ( 'NONE', *, *, #2540, .F. ) ;
#57195=LINE ( 'NONE', #62859, #6797 ) ;
#57309=LINE ( 'NONE', #5819, #13748 ) ;
#57392=DIRECTION ( 'NONE',  ( 0.000000000000000000, 0.000000000000000000, 1.000000000000000000 ) ) ;
#57412=ORIENTED_EDGE ( 'NONE', *, *, #61272, .F. ) ;
#57471=CIRCLE ( 'NONE', #25035, 12.49999999999999822 ) ;
#57501=VECTOR ( 'NONE', #1946, 1000.000000000000000 ) ;
#57543=ORIENTED_EDGE ( 'NONE', *, *, #34011, .T. ) ;
#57563=EDGE_CURVE ( 'NONE', #12963, #32707, #57309, .T. ) ;
#57631=AXIS2_PLACEMENT_3D ( 'NONE', #48561, #30515, #53827 ) ;
#57635=EDGE_CURVE ( 'NONE', #28632, #51981, #62597, .T. ) ;
#57766=DIRECTION ( 'NONE',  ( 1.000000000000000000, 0.000000000000000000, 0.000000000000000000 ) ) ;
#57868=LINE ( 'NONE', #69510, #22183 ) ;
#57913=EDGE_LOOP ( 'NONE', ( #46425, #52172, #47336, #54934, #727 ) ) ;
#57991=SHAPE_DEFINITION_REPRESENTATION ( #45226, #66992 ) ;
#58400=CARTESIAN_POINT ( 'NONE',  ( -12.50000000000000000, -132.5000000000000000, -40.00000000000000000 ) ) ;
#58447=DIRECTION ( 'NONE',  ( -0.000000000000000000, -0.000000000000000000, -1.000000000000000000 ) ) ;
#58709=EDGE_LOOP ( 'NONE', ( #35270, #8591, #20316, #70470, #7268, #35511 ) ) ;
#58924=VERTEX_POINT ( 'NONE', #26076 ) ;
#58999=AXIS2_PLACEMENT_3D ( 'NONE', #48942, #30911, #31288 ) ;
#59025=VERTEX_POINT ( 'NONE', #19692 ) ;
#59349=ORIENTED_EDGE ( 'NONE', *, *, #5311, .T. ) ;
#59750=ORIENTED_EDGE ( 'NONE', *, *, #11483, .F. ) ;
#60075=ORIENTED_EDGE ( 'NONE', *, *, #55163, .T. ) ;
#60114=DIRECTION ( 'NONE',  ( -0.000000000000000000, -0.000000000000000000, -1.000000000000000000 ) ) ;
#60157=CARTESIAN_POINT ( 'NONE',  ( 0.000000000000000000, -120.0000000000000000, -125.0000000000000000 ) ) ;
#60167=AXIS2_PLACEMENT_3D ( 'NONE', #11981, #63878, #28525 ) ;
#60173=DIRECTION ( 'NONE',  ( -1.000000000000000000, 0.000000000000000000, 0.000000000000000000 ) ) ;
#60192=( GEOMETRIC_REPRESENTATION_CONTEXT ( 3 ) GLOBAL_UNCERTAINTY_ASSIGNED_CONTEXT ( ( #49014 ) ) GLOBAL_UNIT_ASSIGNED_CONTEXT ( ( #5073, #45292, #67837 ) ) REPRESENTATION_CONTEXT ( 'NONE', 'WORKASPACE' ) );
#60241=PLANE ( 'NONE',  #65989 ) ;
#60414=DIRECTION ( 'NONE',  ( 1.000000000000000000, 0.000000000000000000, -0.000000000000000000 ) ) ;
#60461=VECTOR ( 'NONE', #63418, 1000.000000000000000 ) ;
#60719=( LENGTH_UNIT ( ) NAMED_UNIT ( * ) SI_UNIT ( .MILLI., .METRE. ) );
#60860=ORIENTED_EDGE ( 'NONE', *, *, #55346, .F. ) ;
#61003=LINE ( 'NONE', #38815, #50428 ) ;
#61027=STYLED_ITEM ( 'NONE', ( #9940 ), #12651 ) ;
#61146=ORIENTED_EDGE ( 'NONE', *, *, #70153, .F. ) ;
#61264=FACE_OUTER_BOUND ( 'NONE', #35845, .T. ) ;
#61272=EDGE_CURVE ( 'NONE', #18300, #51981, #66829, .T. ) ;
#61464=ADVANCED_FACE ( 'NONE', ( #45082 ), #43963, .T. ) ;
#61485=EDGE_LOOP ( 'NONE', ( #41891, #50762, #22450 ) ) ;
#61719=LINE ( 'NONE', #50041, #33678 ) ;
#61803=CARTESIAN_POINT ( 'NONE',  ( 12.50000000000000000, -132.5000000000000000, 40.00000000000000000 ) ) ;
#61835=SURFACE_SIDE_STYLE ('',( #16705 ) ) ;
#62001=DIRECTION ( 'NONE',  ( 0.000000000000000000, 0.000000000000000000, -1.000000000000000000 ) ) ;
#62002=CARTESIAN_POINT ( 'NONE',  ( 0.000000000000000000, -132.5000000000000000, -40.00000000000000711 ) ) ;
#62303=CARTESIAN_POINT ( 'NONE',  ( -12.50000000000000000, -132.5000000000000000, -40.00000000000000000 ) ) ;
#62597=LINE ( 'NONE', #33999, #50953 ) ;
#62607=COLOUR_RGB ( '', 0.72549020, 0.75294118, 0.79215686) ;
#62613=VERTEX_POINT ( 'NONE', #41245 ) ;
#62714=CARTESIAN_POINT ( 'NONE',  ( 0.000000000000000000, -120.0000000000000000, 125.0000000000000000 ) ) ;
#62859=CARTESIAN_POINT ( 'NONE',  ( -12.50000000000000000, -132.5000000000000000, 40.00000000000000000 ) ) ;
#62975=CARTESIAN_POINT ( 'NONE',  ( 0.000000000000000000, -120.0000000000000000, -40.00000000000000711 ) ) ;
#63144=CYLINDRICAL_SURFACE ( 'NONE', #60167, 12.49999999999999822 ) ;
#63274=EDGE_CURVE ( 'NONE', #39300, #53012, #10285, .T. ) ;
#63398=PLANE ( 'NONE',  #43147 ) ;
#63418=DIRECTION ( 'NONE',  ( -1.000000000000000000, -0.000000000000000000, -0.000000000000000000 ) ) ;
#63431=AXIS2_PLACEMENT_3D ( 'NONE', #37103, #20164, #60414 ) ;
#63502=ADVANCED_FACE ( 'NONE', ( #65871 ), #60241, .F. ) ;
#63789=( GEOMETRIC_REPRESENTATION_CONTEXT ( 3 ) GLOBAL_UNCERTAINTY_ASSIGNED_CONTEXT ( ( #15176 ) ) GLOBAL_UNIT_ASSIGNED_CONTEXT ( ( #38524, #10317, #11067 ) ) REPRESENTATION_CONTEXT ( 'NONE', 'WORKASPACE' ) );
#63878=DIRECTION ( 'NONE',  ( -0.000000000000000000, -0.000000000000000000, -1.000000000000000000 ) ) ;
#63905=EDGE_LOOP ( 'NONE', ( #3802, #50898, #717, #32075, #64161, #66215 ) ) ;
#64071=AXIS2_PLACEMENT_3D ( 'NONE', #43707, #49326, #50801 ) ;
#64161=ORIENTED_EDGE ( 'NONE', *, *, #35580, .T. ) ;
#64382=VECTOR ( 'NONE', #27965, 1000.000000000000000 ) ;
#64383=PLANE ( 'NONE',  #57631 ) ;
#64465=CARTESIAN_POINT ( 'NONE',  ( 12.50000000000000000, -132.5000000000000000, -40.00000000000000000 ) ) ;
#64685=CARTESIAN_POINT ( 'NONE',  ( 0.000000000000000000, -120.0000000000000000, 40.00000000000000711 ) ) ;
#65045=VERTEX_POINT ( 'NONE', #51146 ) ;
#65152=CARTESIAN_POINT ( 'NONE',  ( -12.50000000000000000, -132.5000000000000000, 40.00000000000000000 ) ) ;
#65356=DIRECTION ( 'NONE',  ( -1.000000000000000000, -0.000000000000000000, -0.000000000000000000 ) ) ;
#65636=ADVANCED_FACE ( 'NONE', ( #18333 ), #69831, .F. ) ;
#65871=FACE_OUTER_BOUND ( 'NONE', #58709, .T. ) ;
#65989=AXIS2_PLACEMENT_3D ( 'NONE', #30523, #71483, #8721 ) ;
#66137=ADVANCED_FACE ( 'NONE', ( #42211 ), #7616, .F. ) ;
#66215=ORIENTED_EDGE ( 'NONE', *, *, #66871, .F. ) ;
#66792=PRODUCT ( 'output shaft', 'output shaft', '', ( #35058 ) ) ;
#66829=CIRCLE ( 'NONE', #30846, 12.49999999999999822 ) ;
#66871=EDGE_CURVE ( 'NONE', #73511, #62613, #55978, .T. ) ;
#66992=SHAPE_REPRESENTATION ( 'output shaft', ( #43395 ), #60192 ) ;
#67085=FACE_OUTER_BOUND ( 'NONE', #61485, .T. ) ;
#67261=DIRECTION ( 'NONE',  ( -1.000000000000000000, 0.000000000000000000, -0.000000000000000000 ) ) ;
#67396=VERTEX_POINT ( 'NONE', #15675 ) ;
#67535=CIRCLE ( 'NONE', #6315, 12.49999999999999822 ) ;
#67740=DIRECTION ( 'NONE',  ( -1.000000000000000000, 0.000000000000000000, -0.000000000000000000 ) ) ;
#67837=( NAMED_UNIT ( * ) SI_UNIT ( $, .STERADIAN. ) SOLID_ANGLE_UNIT ( ) );
#67848=EDGE_CURVE ( 'NONE', #58924, #39300, #4323, .T. ) ;
#68372=FACE_OUTER_BOUND ( 'NONE', #39664, .T. ) ;
#68699=ADVANCED_BREP_SHAPE_REPRESENTATION ( '', ( #12651, #43395 ), #60192 ) ;
#68707=DIRECTION ( 'NONE',  ( -0.000000000000000000, -0.000000000000000000, -1.000000000000000000 ) ) ;
#68765=CARTESIAN_POINT ( 'NONE',  ( 12.50000000000000000, -132.5000000000000000, 40.00000000000000000 ) ) ;
#68812=ORIENTED_EDGE ( 'NONE', *, *, #70153, .T. ) ;
#68982=ORIENTED_EDGE ( 'NONE', *, *, #2004, .T. ) ;
#69114=DIRECTION ( 'NONE',  ( 0.000000000000000000, -1.000000000000000000, 0.000000000000000000 ) ) ;
#69287=LINE ( 'NONE', #35795, #32577 ) ;
#69510=CARTESIAN_POINT ( 'NONE',  ( -12.50000000000000000, -132.5000000000000000, -40.00000000000000000 ) ) ;
#69831=PLANE ( 'NONE',  #53010 ) ;
#69838=ORIENTED_EDGE ( 'NONE', *, *, #21038, .T. ) ;
#69934=DIRECTION ( 'NONE',  ( 1.000000000000000000, 0.000000000000000000, 0.000000000000000000 ) ) ;
#69952=DIRECTION ( 'NONE',  ( -1.000000000000000000, 0.000000000000000000, 0.000000000000000000 ) ) ;
#70153=EDGE_CURVE ( 'NONE', #51981, #18300, #26200, .T. ) ;
#70312=AXIS2_PLACEMENT_3D ( 'NONE', #30169, #6515, #70753 ) ;
#70470=ORIENTED_EDGE ( 'NONE', *, *, #45154, .T. ) ;
#70753=DIRECTION ( 'NONE',  ( 0.000000000000000000, -0.000000000000000000, 1.000000000000000000 ) ) ;
#71232=DIRECTION ( 'NONE',  ( 0.000000000000000000, 0.000000000000000000, 1.000000000000000000 ) ) ;
#71406=CARTESIAN_POINT ( 'NONE',  ( 0.000000000000000000, -120.0000000000000000, 125.0000000000000000 ) ) ;
#71483=DIRECTION ( 'NONE',  ( -1.000000000000000000, 0.000000000000000000, 0.000000000000000000 ) ) ;
#71873=FACE_OUTER_BOUND ( 'NONE', #41584, .T. ) ;
#71974=SURFACE_SIDE_STYLE ('',( #9199 ) ) ;
#72066=FACE_OUTER_BOUND ( 'NONE', #23065, .T. ) ;
#72466=CYLINDRICAL_SURFACE ( 'NONE', #37448, 12.49999999999999822 ) ;
#72608=EDGE_CURVE ( 'NONE', #58924, #22889, #4769, .T. ) ;
#72969=DIRECTION ( 'NONE',  ( -1.000000000000000000, -0.000000000000000000, -0.000000000000000000 ) ) ;
#73305=CARTESIAN_POINT ( 'NONE',  ( 0.000000000000000000, -120.0000000000000000, 40.00000000000000711 ) ) ;
#73511=VERTEX_POINT ( 'NONE', #68765 ) ;
#74297=DIRECTION ( 'NONE',  ( -1.000000000000000000, 0.000000000000000000, -0.000000000000000000 ) ) ;
ENDSEC;
END-ISO-10303-21;
